ISO-10303-21;
HEADER;
/* Generated by software containing ST-Developer
 * from STEP Tools, Inc. (www.steptools.com) 
 */

FILE_DESCRIPTION(
/* description */ (''),
/* implementation_level */ '2;1');

FILE_NAME(
/* name */ 'Pin_01.step',
/* time_stamp */ '2026-10-04T12:17:52-07:00',
/* author */ (''),
/* organization */ (''),
/* preprocessor_version */ 'ST-DEVELOPER v20.2',
/* originating_system */ 'Autodesk Translation Framework v15.15.0.0',
/* authorisation */ '');

FILE_SCHEMA (('AUTOMOTIVE_DESIGN { 1 0 10303 214 3 1 1 }'));
ENDSEC;

DATA;
#10=MECHANICAL_DESIGN_GEOMETRIC_PRESENTATION_REPRESENTATION('',(#66),#1602);
#50=SHAPE_REPRESENTATION_RELATIONSHIP('SRR','None',#1637,#58);
#58=ADVANCED_BREP_SHAPE_REPRESENTATION('',(#74),#1597);
#66=STYLED_ITEM('',(#1685),#74);
#74=MANIFOLD_SOLID_BREP('Body1',#777);
#117=CIRCLE('',#930,2.5);
#118=CIRCLE('',#932,2.5);
#147=CYLINDRICAL_SURFACE('',#931,2.5);
#184=FACE_OUTER_BOUND('',#239,.T.);
#185=FACE_OUTER_BOUND('',#240,.T.);
#186=FACE_OUTER_BOUND('',#241,.T.);
#239=EDGE_LOOP('',(#654));
#240=EDGE_LOOP('',(#655,#656,#657,#658));
#241=EDGE_LOOP('',(#659));
#304=LINE('',#1518,#353);
#353=VECTOR('',#1138,2.5);
#407=VERTEX_POINT('',#1514);
#408=VERTEX_POINT('',#1517);
#492=EDGE_CURVE('',#407,#407,#117,.T.);
#493=EDGE_CURVE('',#407,#408,#304,.T.);
#494=EDGE_CURVE('',#408,#408,#118,.T.);
#654=ORIENTED_EDGE('',*,*,#492,.T.);
#655=ORIENTED_EDGE('',*,*,#492,.F.);
#656=ORIENTED_EDGE('',*,*,#493,.T.);
#657=ORIENTED_EDGE('',*,*,#494,.T.);
#658=ORIENTED_EDGE('',*,*,#493,.F.);
#659=ORIENTED_EDGE('',*,*,#494,.F.);
#717=PLANE('',#929);
#718=PLANE('',#933);
#756=ADVANCED_FACE('',(#184),#717,.F.);
#757=ADVANCED_FACE('',(#185),#147,.T.);
#758=ADVANCED_FACE('',(#186),#718,.T.);
#777=CLOSED_SHELL('',(#756,#757,#758));
#928=AXIS2_PLACEMENT_3D('',#1512,#1130,#1131);
#929=AXIS2_PLACEMENT_3D('',#1513,#1132,#1133);
#930=AXIS2_PLACEMENT_3D('',#1515,#1134,#1135);
#931=AXIS2_PLACEMENT_3D('',#1516,#1136,#1137);
#932=AXIS2_PLACEMENT_3D('',#1519,#1139,#1140);
#933=AXIS2_PLACEMENT_3D('',#1520,#1141,#1142);
#1130=DIRECTION('axis',(0.,0.,1.));
#1131=DIRECTION('refdir',(1.,0.,0.));
#1132=DIRECTION('center_axis',(0.,1.,0.));
#1133=DIRECTION('ref_axis',(1.,0.,0.));
#1134=DIRECTION('center_axis',(0.,-1.,0.));
#1135=DIRECTION('ref_axis',(1.,0.,0.));
#1136=DIRECTION('center_axis',(0.,-1.,0.));
#1137=DIRECTION('ref_axis',(1.,0.,0.));
#1138=DIRECTION('',(0.,1.,0.));
#1139=DIRECTION('center_axis',(0.,-1.,0.));
#1140=DIRECTION('ref_axis',(1.,0.,0.));
#1141=DIRECTION('center_axis',(0.,1.,0.));
#1142=DIRECTION('ref_axis',(1.,0.,0.));
#1512=CARTESIAN_POINT('',(0.,0.,0.));
#1513=CARTESIAN_POINT('Origin',(11.9313937448893,-8.,61.9313937448893));
#1514=CARTESIAN_POINT('',(9.43139374488932,-8.,61.9313937448893));
#1515=CARTESIAN_POINT('Origin',(11.9313937448893,-8.,61.9313937448893));
#1516=CARTESIAN_POINT('Origin',(11.9313937448893,-3.,61.9313937448893));
#1517=CARTESIAN_POINT('',(9.43139374488932,0.,61.9313937448893));
#1518=CARTESIAN_POINT('',(9.4313937448893,-3.,61.9313937448893));
#1519=CARTESIAN_POINT('Origin',(11.9313937448893,0.,61.9313937448893));
#1520=CARTESIAN_POINT('Origin',(23.8627874897787,0.,50.));
#1587=UNCERTAINTY_MEASURE_WITH_UNIT(LENGTH_MEASURE(0.01),#1603,
'DISTANCE_ACCURACY_VALUE',
'Maximum model space distance between geometric entities at asserted c
onnectivities');
#1592=UNCERTAINTY_MEASURE_WITH_UNIT(LENGTH_MEASURE(0.01),#1603,
'DISTANCE_ACCURACY_VALUE',
'Maximum model space distance between geometric entities at asserted c
onnectivities');
#1597=(
GEOMETRIC_REPRESENTATION_CONTEXT(3)
GLOBAL_UNCERTAINTY_ASSIGNED_CONTEXT((#1587))
GLOBAL_UNIT_ASSIGNED_CONTEXT((#1603,#1605,#1606))
REPRESENTATION_CONTEXT('','3D')
);
#1602=(
GEOMETRIC_REPRESENTATION_CONTEXT(3)
GLOBAL_UNCERTAINTY_ASSIGNED_CONTEXT((#1592))
GLOBAL_UNIT_ASSIGNED_CONTEXT((#1603,#1605,#1606))
REPRESENTATION_CONTEXT('','3D')
);
#1603=(
LENGTH_UNIT()
NAMED_UNIT(*)
SI_UNIT(.MILLI.,.METRE.)
);
#1605=(
NAMED_UNIT(*)
PLANE_ANGLE_UNIT()
SI_UNIT($,.RADIAN.)
);
#1606=(
NAMED_UNIT(*)
SI_UNIT($,.STERADIAN.)
SOLID_ANGLE_UNIT()
);
#1611=SHAPE_DEFINITION_REPRESENTATION(#1620,#1637);
#1620=PRODUCT_DEFINITION_SHAPE('',$,#1647);
#1637=SHAPE_REPRESENTATION('',(#928),#1597);
#1642=PRODUCT_DEFINITION_CONTEXT('part definition',#1671,'design');
#1647=PRODUCT_DEFINITION('Pin_01','Pin_01',#1656,#1642);
#1656=PRODUCT_DEFINITION_FORMATION('',$,#1677);
#1671=APPLICATION_CONTEXT(
'Core Data for Automotive Mechanical Design Process');
#1672=PRODUCT_CONTEXT('part definition',#1671,'mechanical');
#1677=PRODUCT('Pin_01','Pin_01',$,(#1672));
#1685=PRESENTATION_STYLE_ASSIGNMENT((#1689));
#1689=SURFACE_STYLE_USAGE(.BOTH.,#1693);
#1693=SURFACE_SIDE_STYLE('',(#1697));
#1697=SURFACE_STYLE_FILL_AREA(#1701);
#1701=FILL_AREA_STYLE('Opaque(85,255,0)',(#1705));
#1705=FILL_AREA_STYLE_COLOUR('Opaque(85,255,0)',#1709);
#1709=COLOUR_RGB('Opaque(85,255,0)', 0.40784314, 0.44705882, 0.49803922);
ENDSEC;
END-ISO-10303-21;
